ISO-10303-21;
HEADER;
/* Generated by software containing ST-Developer
 * from STEP Tools, Inc. (www.steptools.com) 
 */

FILE_DESCRIPTION(
/* description */ ('Flywheel Crank-Slider'),
/* implementation_level */ '2;1');

FILE_NAME(
/* name */ 'Shaft collar (1).step',
/* time_stamp */ '2026-10-28T03:23:13-07:00',
/* author */ (''),
/* organization */ (''),
/* preprocessor_version */ 'ST-DEVELOPER v20.2',
/* originating_system */ 'Autodesk Translation Framework v15.17.0.0',
/* authorisation */ '');

FILE_SCHEMA (('AUTOMOTIVE_DESIGN { 1 0 10303 214 3 1 1 }'));
ENDSEC;

DATA;
#10=MECHANICAL_DESIGN_GEOMETRIC_PRESENTATION_REPRESENTATION('',(#692),#17322);
#485=B_SPLINE_CURVE_WITH_KNOTS('',3,(#15537,#15538,#15539,#15540,#15541,
#15542,#15543,#15544,#15545,#15546,#15547,#15548,#15549,#15550),
 .UNSPECIFIED.,.F.,.F.,(4,2,2,2,2,2,4),(0.756005737987028,0.793568827564648,
0.872922520054202,0.952276212543757,1.03162990503331,1.11098359752287,1.14854668710049),
 .UNSPECIFIED.);
#486=B_SPLINE_CURVE_WITH_KNOTS('',3,(#15556,#15557,#15558,#15559,#15560,
#15561,#15562,#15563,#15564,#15565,#15566,#15567,#15568,#15569,#15570,#15571,
#15572,#15573),.UNSPECIFIED.,.F.,.F.,(4,2,2,2,2,2,2,2,4),(0.,0.0792165807733633,
0.158433161546727,0.237648697074571,0.316864232602415,0.396079768130259,
0.475295303658103,0.554511884431466,0.63372846520483),.UNSPECIFIED.);
#487=B_SPLINE_CURVE_WITH_KNOTS('',3,(#15574,#15575,#15576,#15577,#15578,
#15579,#15580,#15581,#15582,#15583,#15584,#15585,#15586,#15587,#15588,#15589,
#15590,#15591),.UNSPECIFIED.,.F.,.F.,(4,2,2,2,2,2,2,2,4),(0.63372846520483,
0.712945045978193,0.792161626751556,0.8713771622794,0.950592697807245,1.02980823333509,
1.10902376886293,1.1882403496363,1.26745693040966),.UNSPECIFIED.);
#488=B_SPLINE_CURVE_WITH_KNOTS('',3,(#15594,#15595,#15596,#15597,#15598,
#15599,#15600,#15601,#15602,#15603,#15604,#15605,#15606,#15607),
 .UNSPECIFIED.,.F.,.F.,(4,2,2,2,2,2,4),(0.121154929624524,0.158718019202143,
0.238071711691698,0.317425404181252,0.396779096670807,0.476132789160362,
0.513695878737981),.UNSPECIFIED.);
#587=SHAPE_REPRESENTATION_RELATIONSHIP('SRR','None',#17585,#639);
#639=ADVANCED_BREP_SHAPE_REPRESENTATION('',(#749),#17289);
#692=STYLED_ITEM('',(#17931),#749);
#749=MANIFOLD_SOLID_BREP('Body1',#9074);
#912=FACE_BOUND('',#2275,.T.);
#913=FACE_BOUND('',#2277,.T.);
#914=FACE_BOUND('',#2279,.T.);
#915=FACE_BOUND('',#2281,.T.);
#1185=PLANE('',#10213);
#1186=PLANE('',#10218);
#1187=PLANE('',#10225);
#1188=PLANE('',#10226);
#1609=FACE_OUTER_BOUND('',#2271,.T.);
#1610=FACE_OUTER_BOUND('',#2272,.T.);
#1611=FACE_OUTER_BOUND('',#2273,.T.);
#1612=FACE_OUTER_BOUND('',#2274,.T.);
#1613=FACE_OUTER_BOUND('',#2276,.T.);
#1614=FACE_OUTER_BOUND('',#2278,.T.);
#1615=FACE_OUTER_BOUND('',#2280,.T.);
#2271=EDGE_LOOP('',(#7340,#7341));
#2272=EDGE_LOOP('',(#7342,#7343,#7344,#7345,#7346,#7347,#7348,#7349,#7350));
#2273=EDGE_LOOP('',(#7351,#7352,#7353));
#2274=EDGE_LOOP('',(#7354,#7355,#7356,#7357));
#2275=EDGE_LOOP('',(#7358,#7359,#7360,#7361));
#2276=EDGE_LOOP('',(#7362,#7363,#7364,#7365));
#2277=EDGE_LOOP('',(#7366,#7367));
#2278=EDGE_LOOP('',(#7368));
#2279=EDGE_LOOP('',(#7369));
#2280=EDGE_LOOP('',(#7370));
#2281=EDGE_LOOP('',(#7371));
#2988=LINE('',#15533,#3599);
#2989=LINE('',#15554,#3600);
#2990=LINE('',#15609,#3601);
#2991=LINE('',#15614,#3602);
#2992=LINE('',#15620,#3603);
#3599=VECTOR('',#12260,1.);
#3600=VECTOR('',#12267,0.21);
#3601=VECTOR('',#12272,1.);
#3602=VECTOR('',#12277,1.005);
#3603=VECTOR('',#12284,1.5);
#4047=CIRCLE('',#10214,0.21);
#4048=CIRCLE('',#10216,0.21);
#4049=CIRCLE('',#10217,0.21);
#4050=CIRCLE('',#10220,1.005);
#4051=CIRCLE('',#10221,1.005);
#4052=CIRCLE('',#10223,1.5);
#4053=CIRCLE('',#10224,1.5);
#4680=VERTEX_POINT('',#15531);
#4681=VERTEX_POINT('',#15532);
#4682=VERTEX_POINT('',#15536);
#4683=VERTEX_POINT('',#15551);
#4684=VERTEX_POINT('',#15553);
#4685=VERTEX_POINT('',#15555);
#4686=VERTEX_POINT('',#15592);
#4687=VERTEX_POINT('',#15611);
#4688=VERTEX_POINT('',#15613);
#4689=VERTEX_POINT('',#15617);
#4690=VERTEX_POINT('',#15619);
#5627=EDGE_CURVE('',#4680,#4681,#2988,.T.);
#5628=EDGE_CURVE('',#4680,#4681,#4047,.T.);
#5629=EDGE_CURVE('',#4682,#4680,#485,.T.);
#5630=EDGE_CURVE('',#4683,#4682,#4048,.T.);
#5631=EDGE_CURVE('',#4683,#4684,#2989,.T.);
#5632=EDGE_CURVE('',#4685,#4684,#486,.T.);
#5633=EDGE_CURVE('',#4684,#4685,#487,.T.);
#5634=EDGE_CURVE('',#4686,#4683,#4049,.T.);
#5635=EDGE_CURVE('',#4681,#4686,#488,.T.);
#5636=EDGE_CURVE('',#4686,#4682,#2990,.T.);
#5637=EDGE_CURVE('',#4687,#4687,#4050,.T.);
#5638=EDGE_CURVE('',#4687,#4688,#2991,.T.);
#5639=EDGE_CURVE('',#4688,#4688,#4051,.T.);
#5640=EDGE_CURVE('',#4689,#4689,#4052,.T.);
#5641=EDGE_CURVE('',#4689,#4690,#2992,.T.);
#5642=EDGE_CURVE('',#4690,#4690,#4053,.T.);
#7340=ORIENTED_EDGE('',*,*,#5627,.F.);
#7341=ORIENTED_EDGE('',*,*,#5628,.T.);
#7342=ORIENTED_EDGE('',*,*,#5629,.F.);
#7343=ORIENTED_EDGE('',*,*,#5630,.F.);
#7344=ORIENTED_EDGE('',*,*,#5631,.T.);
#7345=ORIENTED_EDGE('',*,*,#5632,.F.);
#7346=ORIENTED_EDGE('',*,*,#5633,.F.);
#7347=ORIENTED_EDGE('',*,*,#5631,.F.);
#7348=ORIENTED_EDGE('',*,*,#5634,.F.);
#7349=ORIENTED_EDGE('',*,*,#5635,.F.);
#7350=ORIENTED_EDGE('',*,*,#5628,.F.);
#7351=ORIENTED_EDGE('',*,*,#5636,.F.);
#7352=ORIENTED_EDGE('',*,*,#5634,.T.);
#7353=ORIENTED_EDGE('',*,*,#5630,.T.);
#7354=ORIENTED_EDGE('',*,*,#5637,.F.);
#7355=ORIENTED_EDGE('',*,*,#5638,.T.);
#7356=ORIENTED_EDGE('',*,*,#5639,.T.);
#7357=ORIENTED_EDGE('',*,*,#5638,.F.);
#7358=ORIENTED_EDGE('',*,*,#5635,.T.);
#7359=ORIENTED_EDGE('',*,*,#5636,.T.);
#7360=ORIENTED_EDGE('',*,*,#5629,.T.);
#7361=ORIENTED_EDGE('',*,*,#5627,.T.);
#7362=ORIENTED_EDGE('',*,*,#5640,.F.);
#7363=ORIENTED_EDGE('',*,*,#5641,.T.);
#7364=ORIENTED_EDGE('',*,*,#5642,.T.);
#7365=ORIENTED_EDGE('',*,*,#5641,.F.);
#7366=ORIENTED_EDGE('',*,*,#5632,.T.);
#7367=ORIENTED_EDGE('',*,*,#5633,.T.);
#7368=ORIENTED_EDGE('',*,*,#5640,.T.);
#7369=ORIENTED_EDGE('',*,*,#5637,.T.);
#7370=ORIENTED_EDGE('',*,*,#5642,.F.);
#7371=ORIENTED_EDGE('',*,*,#5639,.F.);
#8427=CYLINDRICAL_SURFACE('',#10215,0.21);
#8428=CYLINDRICAL_SURFACE('',#10219,1.005);
#8429=CYLINDRICAL_SURFACE('',#10222,1.5);
#8800=ADVANCED_FACE('',(#1609),#1185,.T.);
#8801=ADVANCED_FACE('',(#1610),#8427,.F.);
#8802=ADVANCED_FACE('',(#1611),#1186,.T.);
#8803=ADVANCED_FACE('',(#1612,#912),#8428,.F.);
#8804=ADVANCED_FACE('',(#1613,#913),#8429,.T.);
#8805=ADVANCED_FACE('',(#1614,#914),#1187,.T.);
#8806=ADVANCED_FACE('',(#1615,#915),#1188,.F.);
#9074=CLOSED_SHELL('',(#8800,#8801,#8802,#8803,#8804,#8805,#8806));
#10212=AXIS2_PLACEMENT_3D('',#15529,#12256,#12257);
#10213=AXIS2_PLACEMENT_3D('',#15530,#12258,#12259);
#10214=AXIS2_PLACEMENT_3D('',#15534,#12261,#12262);
#10215=AXIS2_PLACEMENT_3D('',#15535,#12263,#12264);
#10216=AXIS2_PLACEMENT_3D('',#15552,#12265,#12266);
#10217=AXIS2_PLACEMENT_3D('',#15593,#12268,#12269);
#10218=AXIS2_PLACEMENT_3D('',#15608,#12270,#12271);
#10219=AXIS2_PLACEMENT_3D('',#15610,#12273,#12274);
#10220=AXIS2_PLACEMENT_3D('',#15612,#12275,#12276);
#10221=AXIS2_PLACEMENT_3D('',#15615,#12278,#12279);
#10222=AXIS2_PLACEMENT_3D('',#15616,#12280,#12281);
#10223=AXIS2_PLACEMENT_3D('',#15618,#12282,#12283);
#10224=AXIS2_PLACEMENT_3D('',#15621,#12285,#12286);
#10225=AXIS2_PLACEMENT_3D('',#15622,#12287,#12288);
#10226=AXIS2_PLACEMENT_3D('',#15623,#12289,#12290);
#12256=DIRECTION('axis',(0.,0.,1.));
#12257=DIRECTION('refdir',(1.,0.,0.));
#12258=DIRECTION('center_axis',(0.,0.,1.));
#12259=DIRECTION('ref_axis',(1.,0.,0.));
#12260=DIRECTION('',(0.,1.,0.));
#12261=DIRECTION('center_axis',(0.,0.,1.));
#12262=DIRECTION('ref_axis',(1.,0.,0.));
#12263=DIRECTION('center_axis',(0.,0.,1.));
#12264=DIRECTION('ref_axis',(1.,0.,0.));
#12265=DIRECTION('center_axis',(0.,0.,1.));
#12266=DIRECTION('ref_axis',(1.,0.,0.));
#12267=DIRECTION('',(0.,0.,1.));
#12268=DIRECTION('center_axis',(0.,0.,1.));
#12269=DIRECTION('ref_axis',(1.,0.,0.));
#12270=DIRECTION('center_axis',(0.,0.,1.));
#12271=DIRECTION('ref_axis',(1.,0.,0.));
#12272=DIRECTION('',(0.,-1.,0.));
#12273=DIRECTION('center_axis',(0.,1.,0.));
#12274=DIRECTION('ref_axis',(1.,0.,0.));
#12275=DIRECTION('center_axis',(0.,-1.,0.));
#12276=DIRECTION('ref_axis',(1.,0.,0.));
#12277=DIRECTION('',(0.,-1.,0.));
#12278=DIRECTION('center_axis',(0.,-1.,0.));
#12279=DIRECTION('ref_axis',(1.,0.,0.));
#12280=DIRECTION('center_axis',(0.,1.,0.));
#12281=DIRECTION('ref_axis',(1.,0.,0.));
#12282=DIRECTION('center_axis',(0.,1.,0.));
#12283=DIRECTION('ref_axis',(1.,0.,0.));
#12284=DIRECTION('',(0.,-1.,0.));
#12285=DIRECTION('center_axis',(0.,1.,0.));
#12286=DIRECTION('ref_axis',(1.,0.,0.));
#12287=DIRECTION('center_axis',(0.,1.,0.));
#12288=DIRECTION('ref_axis',(1.,0.,0.));
#12289=DIRECTION('center_axis',(0.,1.,0.));
#12290=DIRECTION('ref_axis',(1.,0.,0.));
#15529=CARTESIAN_POINT('',(0.,0.,0.));
#15530=CARTESIAN_POINT('Origin',(0.,-4.15,10.99));
#15531=CARTESIAN_POINT('',(0.172988438920051,-4.26905880899792,10.99));
#15532=CARTESIAN_POINT('',(0.172988438920051,-4.03094119100208,10.99));
#15533=CARTESIAN_POINT('',(0.172988438920051,-4.55,10.99));
#15534=CARTESIAN_POINT('Origin',(0.,-4.15,10.99));
#15535=CARTESIAN_POINT('Origin',(0.,-4.15,10.99));
#15536=CARTESIAN_POINT('',(-0.172988438920051,-4.26905880899792,10.99));
#15537=CARTESIAN_POINT('Ctrl Pts',(-0.172988438920051,-4.26905880899792,
10.99));
#15538=CARTESIAN_POINT('Ctrl Pts',(-0.165594865311311,-4.2798014223953,
10.9912919219764));
#15539=CARTESIAN_POINT('Ctrl Pts',(-0.157297138725605,-4.28968770937275,
10.992653949439));
#15540=CARTESIAN_POINT('Ctrl Pts',(-0.129892073845076,-4.31709277425327,
10.9967480843909));
#15541=CARTESIAN_POINT('Ctrl Pts',(-0.106330167759284,-4.33324205633295,
10.9996958932764));
#15542=CARTESIAN_POINT('Ctrl Pts',(-0.05461290463241,-4.35469779396491,
11.0038502947236));
#15543=CARTESIAN_POINT('Ctrl Pts',(-0.0264512308298516,-4.36,11.005));
#15544=CARTESIAN_POINT('Ctrl Pts',(0.0264512308298515,-4.36,11.005));
#15545=CARTESIAN_POINT('Ctrl Pts',(0.0546129046324099,-4.35469779396491,
11.0038502947236));
#15546=CARTESIAN_POINT('Ctrl Pts',(0.106330167759284,-4.33324205633295,
10.9996958932764));
#15547=CARTESIAN_POINT('Ctrl Pts',(0.129892073845076,-4.31709277425327,
10.9967480843909));
#15548=CARTESIAN_POINT('Ctrl Pts',(0.157297138725605,-4.28968770937275,
10.992653949439));
#15549=CARTESIAN_POINT('Ctrl Pts',(0.165594865311311,-4.2798014223953,10.9912919219764));
#15550=CARTESIAN_POINT('Ctrl Pts',(0.172988438920051,-4.26905880899792,
10.99));
#15551=CARTESIAN_POINT('',(-0.21,-4.15,10.99));
#15552=CARTESIAN_POINT('Origin',(0.,-4.15,10.99));
#15553=CARTESIAN_POINT('',(-0.21,-4.15,11.4852272553384));
#15554=CARTESIAN_POINT('',(-0.21,-4.15,10.99));
#15555=CARTESIAN_POINT('',(0.21,-4.15,11.4852272553384));
#15556=CARTESIAN_POINT('Ctrl Pts',(0.21,-4.15,11.4852272553384));
#15557=CARTESIAN_POINT('Ctrl Pts',(0.21,-4.17640552692446,11.4852272553384));
#15558=CARTESIAN_POINT('Ctrl Pts',(0.204715737269596,-4.20454707409071,
11.4860041595441));
#15559=CARTESIAN_POINT('Ctrl Pts',(0.183273763036332,-4.25627626890513,
11.4888007328232));
#15560=CARTESIAN_POINT('Ctrl Pts',(0.167117923970394,-4.27986692412796,
11.4907789715758));
#15561=CARTESIAN_POINT('Ctrl Pts',(0.129867169887369,-4.31711767821098,
11.4944848114133));
#15562=CARTESIAN_POINT('Ctrl Pts',(0.106276408305765,-4.33327371000135,
11.4964545565713));
#15563=CARTESIAN_POINT('Ctrl Pts',(0.0545468514059003,-4.35471582482622,
11.4992316551565));
#15564=CARTESIAN_POINT('Ctrl Pts',(0.0264051785092814,-4.36,11.5));
#15565=CARTESIAN_POINT('Ctrl Pts',(-0.0264051785092814,-4.36,11.5));
#15566=CARTESIAN_POINT('Ctrl Pts',(-0.0545468514059002,-4.35471582482622,
11.4992316551565));
#15567=CARTESIAN_POINT('Ctrl Pts',(-0.106276408305765,-4.33327371000135,
11.4964545565713));
#15568=CARTESIAN_POINT('Ctrl Pts',(-0.129867169887369,-4.31711767821098,
11.4944848114133));
#15569=CARTESIAN_POINT('Ctrl Pts',(-0.167117923970394,-4.27986692412796,
11.4907789715758));
#15570=CARTESIAN_POINT('Ctrl Pts',(-0.183273763036332,-4.25627626890513,
11.4888007328232));
#15571=CARTESIAN_POINT('Ctrl Pts',(-0.204715737269596,-4.20454707409071,
11.4860041595441));
#15572=CARTESIAN_POINT('Ctrl Pts',(-0.21,-4.17640552692446,11.4852272553384));
#15573=CARTESIAN_POINT('Ctrl Pts',(-0.21,-4.15,11.4852272553384));
#15574=CARTESIAN_POINT('Ctrl Pts',(-0.21,-4.15,11.4852272553384));
#15575=CARTESIAN_POINT('Ctrl Pts',(-0.21,-4.12359447307555,11.4852272553384));
#15576=CARTESIAN_POINT('Ctrl Pts',(-0.204715737269596,-4.09545292590929,
11.4860041595441));
#15577=CARTESIAN_POINT('Ctrl Pts',(-0.183273763036332,-4.04372373109487,
11.4888007328232));
#15578=CARTESIAN_POINT('Ctrl Pts',(-0.167117923970394,-4.02013307587204,
11.4907789715758));
#15579=CARTESIAN_POINT('Ctrl Pts',(-0.129867169887369,-3.98288232178902,
11.4944848114133));
#15580=CARTESIAN_POINT('Ctrl Pts',(-0.106276408305765,-3.96672628999865,
11.4964545565713));
#15581=CARTESIAN_POINT('Ctrl Pts',(-0.0545468514059,-3.94528417517378,11.4992316551565));
#15582=CARTESIAN_POINT('Ctrl Pts',(-0.0264051785092814,-3.94,11.5));
#15583=CARTESIAN_POINT('Ctrl Pts',(0.0264051785092813,-3.94,11.5));
#15584=CARTESIAN_POINT('Ctrl Pts',(0.0545468514058999,-3.94528417517378,
11.4992316551565));
#15585=CARTESIAN_POINT('Ctrl Pts',(0.106276408305765,-3.96672628999865,
11.4964545565713));
#15586=CARTESIAN_POINT('Ctrl Pts',(0.129867169887369,-3.98288232178902,
11.4944848114133));
#15587=CARTESIAN_POINT('Ctrl Pts',(0.167117923970394,-4.02013307587204,
11.4907789715758));
#15588=CARTESIAN_POINT('Ctrl Pts',(0.183273763036331,-4.04372373109487,
11.4888007328232));
#15589=CARTESIAN_POINT('Ctrl Pts',(0.204715737269596,-4.09545292590929,
11.4860041595441));
#15590=CARTESIAN_POINT('Ctrl Pts',(0.21,-4.12359447307555,11.4852272553384));
#15591=CARTESIAN_POINT('Ctrl Pts',(0.21,-4.15,11.4852272553384));
#15592=CARTESIAN_POINT('',(-0.172988438920051,-4.03094119100208,10.99));
#15593=CARTESIAN_POINT('Origin',(0.,-4.15,10.99));
#15594=CARTESIAN_POINT('Ctrl Pts',(0.172988438920051,-4.03094119100208,
10.99));
#15595=CARTESIAN_POINT('Ctrl Pts',(0.16559486531131,-4.0201985776047,10.9912919219764));
#15596=CARTESIAN_POINT('Ctrl Pts',(0.157297138725604,-4.01031229062725,
10.992653949439));
#15597=CARTESIAN_POINT('Ctrl Pts',(0.129892073845076,-3.98290722574673,
10.9967480843909));
#15598=CARTESIAN_POINT('Ctrl Pts',(0.106330167759284,-3.96675794366705,
10.9996958932764));
#15599=CARTESIAN_POINT('Ctrl Pts',(0.0546129046324106,-3.94530220603509,
11.0038502947236));
#15600=CARTESIAN_POINT('Ctrl Pts',(0.0264512308298516,-3.94,11.005));
#15601=CARTESIAN_POINT('Ctrl Pts',(-0.0264512308298516,-3.94,11.005));
#15602=CARTESIAN_POINT('Ctrl Pts',(-0.0546129046324106,-3.94530220603509,
11.0038502947236));
#15603=CARTESIAN_POINT('Ctrl Pts',(-0.106330167759284,-3.96675794366705,
10.9996958932764));
#15604=CARTESIAN_POINT('Ctrl Pts',(-0.129892073845076,-3.98290722574673,
10.9967480843909));
#15605=CARTESIAN_POINT('Ctrl Pts',(-0.157297138725604,-4.01031229062725,
10.992653949439));
#15606=CARTESIAN_POINT('Ctrl Pts',(-0.16559486531131,-4.0201985776047,10.9912919219764));
#15607=CARTESIAN_POINT('Ctrl Pts',(-0.172988438920051,-4.03094119100208,
10.99));
#15608=CARTESIAN_POINT('Origin',(0.,-4.15,10.99));
#15609=CARTESIAN_POINT('',(-0.172988438920051,-4.55,10.99));
#15610=CARTESIAN_POINT('Origin',(0.,-4.55,10.));
#15611=CARTESIAN_POINT('',(-1.005,-3.75,10.));
#15612=CARTESIAN_POINT('Origin',(0.,-3.75,10.));
#15613=CARTESIAN_POINT('',(-1.005,-4.55,10.));
#15614=CARTESIAN_POINT('',(-1.005,-4.55,10.));
#15615=CARTESIAN_POINT('Origin',(0.,-4.55,10.));
#15616=CARTESIAN_POINT('Origin',(0.,-4.55,10.));
#15617=CARTESIAN_POINT('',(-1.5,-3.75,10.));
#15618=CARTESIAN_POINT('Origin',(0.,-3.75,10.));
#15619=CARTESIAN_POINT('',(-1.5,-4.55,10.));
#15620=CARTESIAN_POINT('',(-1.5,-4.55,10.));
#15621=CARTESIAN_POINT('Origin',(0.,-4.55,10.));
#15622=CARTESIAN_POINT('Origin',(0.,-3.75,10.));
#15623=CARTESIAN_POINT('Origin',(0.,-4.55,10.));
#17228=UNCERTAINTY_MEASURE_WITH_UNIT(LENGTH_MEASURE(0.001),#17323,
'DISTANCE_ACCURACY_VALUE',
'Maximum model space distance between geometric entities at asserted c
onnectivities');
#17261=UNCERTAINTY_MEASURE_WITH_UNIT(LENGTH_MEASURE(0.001),#17323,
'DISTANCE_ACCURACY_VALUE',
'Maximum model space distance between geometric entities at asserted c
onnectivities');
#17289=(
GEOMETRIC_REPRESENTATION_CONTEXT(3)
GLOBAL_UNCERTAINTY_ASSIGNED_CONTEXT((#17228))
GLOBAL_UNIT_ASSIGNED_CONTEXT((#17323,#17325,#17326))
REPRESENTATION_CONTEXT('','3D')
);
#17322=(
GEOMETRIC_REPRESENTATION_CONTEXT(3)
GLOBAL_UNCERTAINTY_ASSIGNED_CONTEXT((#17261))
GLOBAL_UNIT_ASSIGNED_CONTEXT((#17323,#17325,#17326))
REPRESENTATION_CONTEXT('','3D')
);
#17323=(
LENGTH_UNIT()
NAMED_UNIT(*)
SI_UNIT(.CENTI.,.METRE.)
);
#17325=(
NAMED_UNIT(*)
PLANE_ANGLE_UNIT()
SI_UNIT($,.RADIAN.)
);
#17326=(
NAMED_UNIT(*)
SI_UNIT($,.STERADIAN.)
SOLID_ANGLE_UNIT()
);
#17354=SHAPE_DEFINITION_REPRESENTATION(#17416,#17585);
#17416=PRODUCT_DEFINITION_SHAPE('',$,#17646);
#17585=SHAPE_REPRESENTATION('',(#10212),#17289);
#17618=PRODUCT_DEFINITION_CONTEXT('part definition',#17800,'design');
#17646=PRODUCT_DEFINITION('Shaft collar (1)','Shaft collar (1)',#17706,#17618);
#17706=PRODUCT_DEFINITION_FORMATION('',$,#17829);
#17800=APPLICATION_CONTEXT(
'Core Data for Automotive Mechanical Design Process');
#17801=PRODUCT_CONTEXT('part definition',#17800,'mechanical');
#17829=PRODUCT('Shaft collar (1)','Shaft collar (1)','Shaft collar (1)',(#17801));
#17925=COLOUR_RGB('Grey',0.48,0.52,0.57);
#17926=FILL_AREA_STYLE_COLOUR('',#17925);
#17927=FILL_AREA_STYLE('',(#17926));
#17928=SURFACE_STYLE_FILL_AREA(#17927);
#17929=SURFACE_SIDE_STYLE('',(#17928));
#17930=SURFACE_STYLE_USAGE(.BOTH.,#17929);
#17931=PRESENTATION_STYLE_ASSIGNMENT((#17930));
ENDSEC;
END-ISO-10303-21;
